ISO-10303-21;
HEADER;
/* Generated by software containing ST-Developer
 * from STEP Tools, Inc. (www.steptools.com) 
 */

FILE_DESCRIPTION(
/* description */ ('Belt conveyor head drive unit'),
/* implementation_level */ '2;1');

FILE_NAME(
/* name */ 'Socket Set Screw - M5x8.step',
/* time_stamp */ '2026-10-28T03:26:19-07:00',
/* author */ (''),
/* organization */ (''),
/* preprocessor_version */ 'ST-DEVELOPER v20.2',
/* originating_system */ 'Autodesk Translation Framework v15.17.0.0',
/* authorisation */ '');

FILE_SCHEMA (('AUTOMOTIVE_DESIGN { 1 0 10303 214 3 1 1 }'));
ENDSEC;

DATA;
#10=MECHANICAL_DESIGN_GEOMETRIC_PRESENTATION_REPRESENTATION('',(#931),#27069);
#703=CONICAL_SURFACE('',#16393,0.235,0.785398163397448);
#704=CONICAL_SURFACE('',#16397,0.2125,0.785398163397448);
#777=SHAPE_REPRESENTATION_RELATIONSHIP('SRR','None',#27426,#846);
#846=ADVANCED_BREP_SHAPE_REPRESENTATION('',(#1011),#27068);
#931=STYLED_ITEM('',(#27804),#1011);
#1011=MANIFOLD_SOLID_BREP('Body1',#13801);
#1276=FACE_BOUND('',#3493,.T.);
#1624=PLANE('',#16384);
#1625=PLANE('',#16385);
#1626=PLANE('',#16386);
#1627=PLANE('',#16387);
#1628=PLANE('',#16388);
#1629=PLANE('',#16389);
#1630=PLANE('',#16390);
#1631=PLANE('',#16391);
#1632=PLANE('',#16399);
#2421=FACE_OUTER_BOUND('',#3485,.T.);
#2422=FACE_OUTER_BOUND('',#3486,.T.);
#2423=FACE_OUTER_BOUND('',#3487,.T.);
#2424=FACE_OUTER_BOUND('',#3488,.T.);
#2425=FACE_OUTER_BOUND('',#3489,.T.);
#2426=FACE_OUTER_BOUND('',#3490,.T.);
#2427=FACE_OUTER_BOUND('',#3491,.T.);
#2428=FACE_OUTER_BOUND('',#3492,.T.);
#2429=FACE_OUTER_BOUND('',#3494,.T.);
#2430=FACE_OUTER_BOUND('',#3495,.T.);
#2431=FACE_OUTER_BOUND('',#3496,.T.);
#2432=FACE_OUTER_BOUND('',#3497,.T.);
#3485=EDGE_LOOP('',(#12482,#12483,#12484,#12485));
#3486=EDGE_LOOP('',(#12486,#12487,#12488,#12489));
#3487=EDGE_LOOP('',(#12490,#12491,#12492,#12493));
#3488=EDGE_LOOP('',(#12494,#12495,#12496,#12497));
#3489=EDGE_LOOP('',(#12498,#12499,#12500,#12501));
#3490=EDGE_LOOP('',(#12502,#12503,#12504,#12505));
#3491=EDGE_LOOP('',(#12506,#12507,#12508,#12509,#12510,#12511));
#3492=EDGE_LOOP('',(#12512));
#3493=EDGE_LOOP('',(#12513,#12514,#12515,#12516,#12517,#12518));
#3494=EDGE_LOOP('',(#12519,#12520,#12521,#12522));
#3495=EDGE_LOOP('',(#12523,#12524,#12525,#12526));
#3496=EDGE_LOOP('',(#12527,#12528,#12529,#12530));
#3497=EDGE_LOOP('',(#12531));
#4269=LINE('',#26832,#5061);
#4270=LINE('',#26834,#5062);
#4271=LINE('',#26836,#5063);
#4272=LINE('',#26837,#5064);
#4273=LINE('',#26840,#5065);
#4274=LINE('',#26842,#5066);
#4275=LINE('',#26843,#5067);
#4276=LINE('',#26846,#5068);
#4277=LINE('',#26848,#5069);
#4278=LINE('',#26849,#5070);
#4279=LINE('',#26852,#5071);
#4280=LINE('',#26854,#5072);
#4281=LINE('',#26855,#5073);
#4282=LINE('',#26858,#5074);
#4283=LINE('',#26860,#5075);
#4284=LINE('',#26861,#5076);
#4285=LINE('',#26863,#5077);
#4286=LINE('',#26864,#5078);
#4287=LINE('',#26872,#5079);
#4288=LINE('',#26876,#5080);
#4289=LINE('',#26880,#5081);
#5061=VECTOR('',#20851,1.);
#5062=VECTOR('',#20852,1.);
#5063=VECTOR('',#20853,1.);
#5064=VECTOR('',#20854,1.);
#5065=VECTOR('',#20857,1.);
#5066=VECTOR('',#20858,1.);
#5067=VECTOR('',#20859,1.);
#5068=VECTOR('',#20862,1.);
#5069=VECTOR('',#20863,1.);
#5070=VECTOR('',#20864,1.);
#5071=VECTOR('',#20867,1.);
#5072=VECTOR('',#20868,1.);
#5073=VECTOR('',#20869,1.);
#5074=VECTOR('',#20872,1.);
#5075=VECTOR('',#20873,1.);
#5076=VECTOR('',#20874,1.);
#5077=VECTOR('',#20877,1.);
#5078=VECTOR('',#20878,1.);
#5079=VECTOR('',#20889,0.235);
#5080=VECTOR('',#20894,0.25);
#5081=VECTOR('',#20899,0.2125);
#5949=CIRCLE('',#16392,0.22);
#5950=CIRCLE('',#16394,0.24505);
#5951=CIRCLE('',#16396,0.24505);
#5952=CIRCLE('',#16398,0.175);
#7155=VERTEX_POINT('',#26830);
#7156=VERTEX_POINT('',#26831);
#7157=VERTEX_POINT('',#26833);
#7158=VERTEX_POINT('',#26835);
#7159=VERTEX_POINT('',#26839);
#7160=VERTEX_POINT('',#26841);
#7161=VERTEX_POINT('',#26845);
#7162=VERTEX_POINT('',#26847);
#7163=VERTEX_POINT('',#26851);
#7164=VERTEX_POINT('',#26853);
#7165=VERTEX_POINT('',#26857);
#7166=VERTEX_POINT('',#26859);
#7167=VERTEX_POINT('',#26867);
#7168=VERTEX_POINT('',#26870);
#7169=VERTEX_POINT('',#26874);
#7170=VERTEX_POINT('',#26878);
#8933=EDGE_CURVE('',#7155,#7156,#4269,.T.);
#8934=EDGE_CURVE('',#7155,#7157,#4270,.T.);
#8935=EDGE_CURVE('',#7157,#7158,#4271,.T.);
#8936=EDGE_CURVE('',#7156,#7158,#4272,.T.);
#8937=EDGE_CURVE('',#7159,#7155,#4273,.T.);
#8938=EDGE_CURVE('',#7159,#7160,#4274,.T.);
#8939=EDGE_CURVE('',#7160,#7157,#4275,.T.);
#8940=EDGE_CURVE('',#7161,#7159,#4276,.T.);
#8941=EDGE_CURVE('',#7161,#7162,#4277,.T.);
#8942=EDGE_CURVE('',#7162,#7160,#4278,.T.);
#8943=EDGE_CURVE('',#7163,#7161,#4279,.T.);
#8944=EDGE_CURVE('',#7163,#7164,#4280,.T.);
#8945=EDGE_CURVE('',#7164,#7162,#4281,.T.);
#8946=EDGE_CURVE('',#7165,#7163,#4282,.T.);
#8947=EDGE_CURVE('',#7165,#7166,#4283,.T.);
#8948=EDGE_CURVE('',#7166,#7164,#4284,.T.);
#8949=EDGE_CURVE('',#7156,#7165,#4285,.T.);
#8950=EDGE_CURVE('',#7158,#7166,#4286,.T.);
#8951=EDGE_CURVE('',#7167,#7167,#5949,.T.);
#8952=EDGE_CURVE('',#7168,#7168,#5950,.T.);
#8953=EDGE_CURVE('',#7168,#7167,#4287,.T.);
#8954=EDGE_CURVE('',#7169,#7169,#5951,.F.);
#8955=EDGE_CURVE('',#7169,#7168,#4288,.T.);
#8956=EDGE_CURVE('',#7170,#7170,#5952,.T.);
#8957=EDGE_CURVE('',#7170,#7169,#4289,.T.);
#12482=ORIENTED_EDGE('',*,*,#8933,.F.);
#12483=ORIENTED_EDGE('',*,*,#8934,.T.);
#12484=ORIENTED_EDGE('',*,*,#8935,.T.);
#12485=ORIENTED_EDGE('',*,*,#8936,.F.);
#12486=ORIENTED_EDGE('',*,*,#8937,.F.);
#12487=ORIENTED_EDGE('',*,*,#8938,.T.);
#12488=ORIENTED_EDGE('',*,*,#8939,.T.);
#12489=ORIENTED_EDGE('',*,*,#8934,.F.);
#12490=ORIENTED_EDGE('',*,*,#8940,.F.);
#12491=ORIENTED_EDGE('',*,*,#8941,.T.);
#12492=ORIENTED_EDGE('',*,*,#8942,.T.);
#12493=ORIENTED_EDGE('',*,*,#8938,.F.);
#12494=ORIENTED_EDGE('',*,*,#8943,.F.);
#12495=ORIENTED_EDGE('',*,*,#8944,.T.);
#12496=ORIENTED_EDGE('',*,*,#8945,.T.);
#12497=ORIENTED_EDGE('',*,*,#8941,.F.);
#12498=ORIENTED_EDGE('',*,*,#8946,.F.);
#12499=ORIENTED_EDGE('',*,*,#8947,.T.);
#12500=ORIENTED_EDGE('',*,*,#8948,.T.);
#12501=ORIENTED_EDGE('',*,*,#8944,.F.);
#12502=ORIENTED_EDGE('',*,*,#8949,.F.);
#12503=ORIENTED_EDGE('',*,*,#8936,.T.);
#12504=ORIENTED_EDGE('',*,*,#8950,.T.);
#12505=ORIENTED_EDGE('',*,*,#8947,.F.);
#12506=ORIENTED_EDGE('',*,*,#8950,.F.);
#12507=ORIENTED_EDGE('',*,*,#8935,.F.);
#12508=ORIENTED_EDGE('',*,*,#8939,.F.);
#12509=ORIENTED_EDGE('',*,*,#8942,.F.);
#12510=ORIENTED_EDGE('',*,*,#8945,.F.);
#12511=ORIENTED_EDGE('',*,*,#8948,.F.);
#12512=ORIENTED_EDGE('',*,*,#8951,.F.);
#12513=ORIENTED_EDGE('',*,*,#8933,.T.);
#12514=ORIENTED_EDGE('',*,*,#8949,.T.);
#12515=ORIENTED_EDGE('',*,*,#8946,.T.);
#12516=ORIENTED_EDGE('',*,*,#8943,.T.);
#12517=ORIENTED_EDGE('',*,*,#8940,.T.);
#12518=ORIENTED_EDGE('',*,*,#8937,.T.);
#12519=ORIENTED_EDGE('',*,*,#8952,.F.);
#12520=ORIENTED_EDGE('',*,*,#8953,.T.);
#12521=ORIENTED_EDGE('',*,*,#8951,.T.);
#12522=ORIENTED_EDGE('',*,*,#8953,.F.);
#12523=ORIENTED_EDGE('',*,*,#8954,.F.);
#12524=ORIENTED_EDGE('',*,*,#8955,.T.);
#12525=ORIENTED_EDGE('',*,*,#8952,.T.);
#12526=ORIENTED_EDGE('',*,*,#8955,.F.);
#12527=ORIENTED_EDGE('',*,*,#8956,.F.);
#12528=ORIENTED_EDGE('',*,*,#8957,.T.);
#12529=ORIENTED_EDGE('',*,*,#8954,.T.);
#12530=ORIENTED_EDGE('',*,*,#8957,.F.);
#12531=ORIENTED_EDGE('',*,*,#8956,.T.);
#12911=CYLINDRICAL_SURFACE('',#16395,0.24505);
#13700=ADVANCED_FACE('',(#2421),#1624,.F.);
#13701=ADVANCED_FACE('',(#2422),#1625,.F.);
#13702=ADVANCED_FACE('',(#2423),#1626,.F.);
#13703=ADVANCED_FACE('',(#2424),#1627,.F.);
#13704=ADVANCED_FACE('',(#2425),#1628,.F.);
#13705=ADVANCED_FACE('',(#2426),#1629,.F.);
#13706=ADVANCED_FACE('',(#2427),#1630,.F.);
#13707=ADVANCED_FACE('',(#2428,#1276),#1631,.T.);
#13708=ADVANCED_FACE('',(#2429),#703,.T.);
#13709=ADVANCED_FACE('',(#2430),#12911,.T.);
#13710=ADVANCED_FACE('',(#2431),#704,.T.);
#13711=ADVANCED_FACE('',(#2432),#1632,.T.);
#13801=CLOSED_SHELL('',(#13700,#13701,#13702,#13703,#13704,#13705,#13706,
#13707,#13708,#13709,#13710,#13711));
#16383=AXIS2_PLACEMENT_3D('',#26828,#20847,#20848);
#16384=AXIS2_PLACEMENT_3D('',#26829,#20849,#20850);
#16385=AXIS2_PLACEMENT_3D('',#26838,#20855,#20856);
#16386=AXIS2_PLACEMENT_3D('',#26844,#20860,#20861);
#16387=AXIS2_PLACEMENT_3D('',#26850,#20865,#20866);
#16388=AXIS2_PLACEMENT_3D('',#26856,#20870,#20871);
#16389=AXIS2_PLACEMENT_3D('',#26862,#20875,#20876);
#16390=AXIS2_PLACEMENT_3D('',#26865,#20879,#20880);
#16391=AXIS2_PLACEMENT_3D('',#26866,#20881,#20882);
#16392=AXIS2_PLACEMENT_3D('',#26868,#20883,#20884);
#16393=AXIS2_PLACEMENT_3D('',#26869,#20885,#20886);
#16394=AXIS2_PLACEMENT_3D('',#26871,#20887,#20888);
#16395=AXIS2_PLACEMENT_3D('',#26873,#20890,#20891);
#16396=AXIS2_PLACEMENT_3D('',#26875,#20892,#20893);
#16397=AXIS2_PLACEMENT_3D('',#26877,#20895,#20896);
#16398=AXIS2_PLACEMENT_3D('',#26879,#20897,#20898);
#16399=AXIS2_PLACEMENT_3D('',#26881,#20900,#20901);
#20847=DIRECTION('axis',(0.,0.,1.));
#20848=DIRECTION('refdir',(1.,0.,0.));
#20849=DIRECTION('center_axis',(0.866025403784439,0.,-0.5));
#20850=DIRECTION('ref_axis',(0.5,0.,0.866025403784439));
#20851=DIRECTION('',(0.5,0.,0.866025403784439));
#20852=DIRECTION('',(0.,-1.,0.));
#20853=DIRECTION('',(0.5,0.,0.866025403784439));
#20854=DIRECTION('',(0.,-1.,0.));
#20855=DIRECTION('center_axis',(1.92296268638356E-16,0.,-1.));
#20856=DIRECTION('ref_axis',(1.,0.,1.92296268638356E-16));
#20857=DIRECTION('',(1.,0.,1.92296268638356E-16));
#20858=DIRECTION('',(0.,-1.,0.));
#20859=DIRECTION('',(1.,0.,1.92296268638356E-16));
#20860=DIRECTION('center_axis',(-0.866025403784439,0.,-0.5));
#20861=DIRECTION('ref_axis',(0.5,0.,-0.866025403784439));
#20862=DIRECTION('',(0.5,0.,-0.866025403784439));
#20863=DIRECTION('',(0.,-1.,0.));
#20864=DIRECTION('',(0.5,0.,-0.866025403784438));
#20865=DIRECTION('center_axis',(-0.866025403784439,0.,0.5));
#20866=DIRECTION('ref_axis',(-0.5,0.,-0.866025403784439));
#20867=DIRECTION('',(-0.5,0.,-0.866025403784439));
#20868=DIRECTION('',(0.,-1.,0.));
#20869=DIRECTION('',(-0.5,0.,-0.866025403784439));
#20870=DIRECTION('center_axis',(-1.92296268638356E-16,0.,1.));
#20871=DIRECTION('ref_axis',(-1.,0.,-1.92296268638356E-16));
#20872=DIRECTION('',(-1.,0.,-1.92296268638356E-16));
#20873=DIRECTION('',(0.,-1.,0.));
#20874=DIRECTION('',(-1.,0.,-1.92296268638356E-16));
#20875=DIRECTION('center_axis',(0.866025403784439,0.,0.5));
#20876=DIRECTION('ref_axis',(-0.5,0.,0.866025403784439));
#20877=DIRECTION('',(-0.5,0.,0.866025403784439));
#20878=DIRECTION('',(-0.5,0.,0.866025403784439));
#20879=DIRECTION('center_axis',(0.,-1.,0.));
#20880=DIRECTION('ref_axis',(0.,0.,-1.));
#20881=DIRECTION('center_axis',(0.,1.,0.));
#20882=DIRECTION('ref_axis',(0.,0.,1.));
#20883=DIRECTION('center_axis',(0.,-1.,0.));
#20884=DIRECTION('ref_axis',(1.,0.,0.));
#20885=DIRECTION('center_axis',(0.,-1.,0.));
#20886=DIRECTION('ref_axis',(1.,0.,0.));
#20887=DIRECTION('center_axis',(0.,-1.,0.));
#20888=DIRECTION('ref_axis',(1.,0.,0.));
#20889=DIRECTION('',(0.707106781186547,0.707106781186548,8.65956056235493E-17));
#20890=DIRECTION('center_axis',(0.,-1.,0.));
#20891=DIRECTION('ref_axis',(1.,0.,0.));
#20892=DIRECTION('center_axis',(0.,1.,0.));
#20893=DIRECTION('ref_axis',(1.,0.,0.));
#20894=DIRECTION('',(0.,1.,0.));
#20895=DIRECTION('center_axis',(0.,1.,0.));
#20896=DIRECTION('ref_axis',(1.,0.,0.));
#20897=DIRECTION('center_axis',(0.,-1.,0.));
#20898=DIRECTION('ref_axis',(1.,0.,0.));
#20899=DIRECTION('',(-0.707106781186547,0.707106781186548,-8.65956056235493E-17));
#20900=DIRECTION('center_axis',(0.,-1.,0.));
#20901=DIRECTION('ref_axis',(0.,0.,-1.));
#26828=CARTESIAN_POINT('',(0.,0.,0.));
#26829=CARTESIAN_POINT('Origin',(0.0721687836487032,0.,-0.125));
#26830=CARTESIAN_POINT('',(0.0721687836487032,0.,-0.125));
#26831=CARTESIAN_POINT('',(0.144337567297406,0.,0.));
#26832=CARTESIAN_POINT('',(0.117710979560879,0.,-0.0461186027918559));
#26833=CARTESIAN_POINT('',(0.0721687836487032,-0.25,-0.125));
#26834=CARTESIAN_POINT('',(0.0721687836487032,0.,-0.125));
#26835=CARTESIAN_POINT('',(0.144337567297406,-0.25,0.));
#26836=CARTESIAN_POINT('',(0.144337567297406,-0.25,0.));
#26837=CARTESIAN_POINT('',(0.144337567297406,0.,0.));
#26838=CARTESIAN_POINT('Origin',(-0.0721687836487032,0.,-0.125));
#26839=CARTESIAN_POINT('',(-0.0721687836487032,0.,-0.125));
#26840=CARTESIAN_POINT('',(0.0739156081756484,0.,-0.125));
#26841=CARTESIAN_POINT('',(-0.0721687836487032,-0.25,-0.125));
#26842=CARTESIAN_POINT('',(-0.0721687836487032,0.,-0.125));
#26843=CARTESIAN_POINT('',(0.0721687836487032,-0.25,-0.125));
#26844=CARTESIAN_POINT('Origin',(-0.144337567297406,0.,-4.16333634234434E-17));
#26845=CARTESIAN_POINT('',(-0.144337567297406,0.,-1.76762539787485E-17));
#26846=CARTESIAN_POINT('',(-0.0987953713852306,0.,-0.0788813972081442));
#26847=CARTESIAN_POINT('',(-0.144337567297406,-0.25,-2.77555756156289E-17));
#26848=CARTESIAN_POINT('',(-0.144337567297406,0.,-1.76762539787485E-17));
#26849=CARTESIAN_POINT('',(-0.0721687836487032,-0.25,-0.125));
#26850=CARTESIAN_POINT('Origin',(-0.0721687836487033,0.,0.125));
#26851=CARTESIAN_POINT('',(-0.0721687836487033,0.,0.125));
#26852=CARTESIAN_POINT('',(-0.0627109795608791,0.,0.141381397208144));
#26853=CARTESIAN_POINT('',(-0.0721687836487033,-0.25,0.125));
#26854=CARTESIAN_POINT('',(-0.0721687836487033,0.,0.125));
#26855=CARTESIAN_POINT('',(-0.144337567297406,-0.25,-1.76762539787485E-17));
#26856=CARTESIAN_POINT('Origin',(0.0721687836487032,0.,0.125));
#26857=CARTESIAN_POINT('',(0.0721687836487032,0.,0.125));
#26858=CARTESIAN_POINT('',(0.146084391824352,0.,0.125));
#26859=CARTESIAN_POINT('',(0.0721687836487032,-0.25,0.125));
#26860=CARTESIAN_POINT('',(0.0721687836487032,0.,0.125));
#26861=CARTESIAN_POINT('',(-0.0721687836487033,-0.25,0.125));
#26862=CARTESIAN_POINT('Origin',(0.144337567297406,0.,0.));
#26863=CARTESIAN_POINT('',(0.153795371385231,0.,-0.0163813972081441));
#26864=CARTESIAN_POINT('',(0.0721687836487032,-0.25,0.125));
#26865=CARTESIAN_POINT('Origin',(0.,-0.25,0.));
#26866=CARTESIAN_POINT('Origin',(0.22,0.,0.));
#26867=CARTESIAN_POINT('',(-0.22,-8.67361737988404E-18,-2.69422295812418E-17));
#26868=CARTESIAN_POINT('Origin',(0.,0.,0.));
#26869=CARTESIAN_POINT('Origin',(0.,-0.015,0.));
#26870=CARTESIAN_POINT('',(-0.24505,-0.02505,-3.00099698131059E-17));
#26871=CARTESIAN_POINT('Origin',(0.,-0.02505,0.));
#26872=CARTESIAN_POINT('',(-0.235,-0.015,-2.87791997799628E-17));
#26873=CARTESIAN_POINT('Origin',(0.,-0.3775,0.));
#26874=CARTESIAN_POINT('',(-0.24505,-0.72995,3.00099698131059E-17));
#26875=CARTESIAN_POINT('Origin',(0.,-0.72995,0.));
#26876=CARTESIAN_POINT('',(-0.24505,-0.3775,-3.00099698131059E-17));
#26877=CARTESIAN_POINT('Origin',(0.,-0.7625,0.));
#26878=CARTESIAN_POINT('',(-0.175,-0.8,-2.14313189850787E-17));
#26879=CARTESIAN_POINT('Origin',(0.,-0.8,0.));
#26880=CARTESIAN_POINT('',(-0.2125,-0.7625,-2.60237444818813E-17));
#26881=CARTESIAN_POINT('Origin',(0.,-0.8,0.));
#26991=UNCERTAINTY_MEASURE_WITH_UNIT(LENGTH_MEASURE(0.001),#27070,
'DISTANCE_ACCURACY_VALUE',
'Maximum model space distance between geometric entities at asserted c
onnectivities');
#26992=UNCERTAINTY_MEASURE_WITH_UNIT(LENGTH_MEASURE(0.001),#27070,
'DISTANCE_ACCURACY_VALUE',
'Maximum model space distance between geometric entities at asserted c
onnectivities');
#27068=(
GEOMETRIC_REPRESENTATION_CONTEXT(3)
GLOBAL_UNCERTAINTY_ASSIGNED_CONTEXT((#26991))
GLOBAL_UNIT_ASSIGNED_CONTEXT((#27070,#27072,#27073))
REPRESENTATION_CONTEXT('','3D')
);
#27069=(
GEOMETRIC_REPRESENTATION_CONTEXT(3)
GLOBAL_UNCERTAINTY_ASSIGNED_CONTEXT((#26992))
GLOBAL_UNIT_ASSIGNED_CONTEXT((#27070,#27072,#27073))
REPRESENTATION_CONTEXT('','3D')
);
#27070=(
LENGTH_UNIT()
NAMED_UNIT(*)
SI_UNIT(.CENTI.,.METRE.)
);
#27072=(
NAMED_UNIT(*)
PLANE_ANGLE_UNIT()
SI_UNIT($,.RADIAN.)
);
#27073=(
NAMED_UNIT(*)
SI_UNIT($,.STERADIAN.)
SOLID_ANGLE_UNIT()
);
#27149=SHAPE_DEFINITION_REPRESENTATION(#27316,#27426);
#27316=PRODUCT_DEFINITION_SHAPE('',$,#27503);
#27426=SHAPE_REPRESENTATION('',(#16383),#27068);
#27427=PRODUCT_DEFINITION_CONTEXT('part definition',#27657,'design');
#27503=PRODUCT_DEFINITION('Socket Set Screw - M5x8',
'Socket Set Screw - M5x8',#27579,#27427);
#27579=PRODUCT_DEFINITION_FORMATION('',$,#27734);
#27657=APPLICATION_CONTEXT(
'Core Data for Automotive Mechanical Design Process');
#27658=PRODUCT_CONTEXT('part definition',#27657,'mechanical');
#27734=PRODUCT('Socket Set Screw - M5x8','Socket Set Screw - M5x8',
'Socket Set Screw - M5x8',(#27658));
#27798=COLOUR_RGB('Black',0.12,0.14,0.17);
#27799=FILL_AREA_STYLE_COLOUR('',#27798);
#27800=FILL_AREA_STYLE('',(#27799));
#27801=SURFACE_STYLE_FILL_AREA(#27800);
#27802=SURFACE_SIDE_STYLE('',(#27801));
#27803=SURFACE_STYLE_USAGE(.BOTH.,#27802);
#27804=PRESENTATION_STYLE_ASSIGNMENT((#27803));
ENDSEC;
END-ISO-10303-21;
